ISO-10303-21;
HEADER;
/* Generated by software containing ST-Developer
 * from STEP Tools, Inc. (www.steptools.com) 
 */

FILE_DESCRIPTION(
/* description */ ('Bearing friction torque test rig'),
/* implementation_level */ '2;1');

FILE_NAME(
/* name */ 'Inner ring (1).step',
/* time_stamp */ '2026-10-28T03:24:04-07:00',
/* author */ (''),
/* organization */ (''),
/* preprocessor_version */ 'ST-DEVELOPER v20.2',
/* originating_system */ 'Autodesk Translation Framework v15.17.0.0',
/* authorisation */ '');

FILE_SCHEMA (('AUTOMOTIVE_DESIGN { 1 0 10303 214 3 1 1 }'));
ENDSEC;

DATA;
#10=MECHANICAL_DESIGN_GEOMETRIC_PRESENTATION_REPRESENTATION('',(#567),#14822);
#427=TOROIDAL_SURFACE('',#8752,1.675,0.412776);
#436=CONICAL_SURFACE('',#8763,1.05,0.785398163397449);
#437=CONICAL_SURFACE('',#8770,1.05,0.785398163397449);
#482=SHAPE_REPRESENTATION_RELATIONSHIP('SRR','None',#15023,#521);
#521=ADVANCED_BREP_SHAPE_REPRESENTATION('',(#620),#14803);
#567=STYLED_ITEM('',(#15284),#620);
#620=MANIFOLD_SOLID_BREP('Body1',#7684);
#823=FACE_BOUND('',#2013,.T.);
#824=FACE_BOUND('',#2016,.T.);
#1018=PLANE('',#8765);
#1019=PLANE('',#8768);
#1384=FACE_OUTER_BOUND('',#2008,.T.);
#1385=FACE_OUTER_BOUND('',#2009,.T.);
#1386=FACE_OUTER_BOUND('',#2010,.T.);
#1387=FACE_OUTER_BOUND('',#2011,.T.);
#1388=FACE_OUTER_BOUND('',#2012,.T.);
#1389=FACE_OUTER_BOUND('',#2014,.T.);
#1390=FACE_OUTER_BOUND('',#2015,.T.);
#1391=FACE_OUTER_BOUND('',#2017,.T.);
#2008=EDGE_LOOP('',(#6402,#6403,#6404,#6405,#6406,#6407));
#2009=EDGE_LOOP('',(#6408,#6409,#6410,#6411,#6412));
#2010=EDGE_LOOP('',(#6413,#6414,#6415,#6416));
#2011=EDGE_LOOP('',(#6417,#6418,#6419,#6420));
#2012=EDGE_LOOP('',(#6421));
#2013=EDGE_LOOP('',(#6422));
#2014=EDGE_LOOP('',(#6423,#6424,#6425,#6426,#6427));
#2015=EDGE_LOOP('',(#6428));
#2016=EDGE_LOOP('',(#6429));
#2017=EDGE_LOOP('',(#6430,#6431,#6432,#6433));
#2538=LINE('',#13332,#2982);
#2539=LINE('',#13338,#2983);
#2540=LINE('',#13342,#2984);
#2541=LINE('',#13348,#2985);
#2542=LINE('',#13353,#2986);
#2982=VECTOR('',#10719,1.63531);
#2983=VECTOR('',#10726,1.);
#2984=VECTOR('',#10731,1.05);
#2985=VECTOR('',#10740,1.63531);
#2986=VECTOR('',#10747,1.05);
#3395=CIRCLE('',#8753,1.63531);
#3396=CIRCLE('',#8754,1.63531);
#3397=CIRCLE('',#8755,0.412776);
#3398=CIRCLE('',#8756,1.63531);
#3399=CIRCLE('',#8757,1.63531);
#3400=CIRCLE('',#8759,1.63531);
#3401=CIRCLE('',#8761,1.);
#3402=CIRCLE('',#8762,1.);
#3403=CIRCLE('',#8764,1.1);
#3404=CIRCLE('',#8767,1.63531);
#3405=CIRCLE('',#8769,1.1);
#3978=VERTEX_POINT('',#13321);
#3979=VERTEX_POINT('',#13322);
#3980=VERTEX_POINT('',#13325);
#3981=VERTEX_POINT('',#13327);
#3982=VERTEX_POINT('',#13331);
#3983=VERTEX_POINT('',#13335);
#3984=VERTEX_POINT('',#13337);
#3985=VERTEX_POINT('',#13341);
#3986=VERTEX_POINT('',#13346);
#3987=VERTEX_POINT('',#13350);
#4827=EDGE_CURVE('',#3978,#3979,#3395,.T.);
#4828=EDGE_CURVE('',#3979,#3978,#3396,.T.);
#4829=EDGE_CURVE('',#3979,#3980,#3397,.T.);
#4830=EDGE_CURVE('',#3981,#3980,#3398,.T.);
#4831=EDGE_CURVE('',#3980,#3981,#3399,.T.);
#4832=EDGE_CURVE('',#3981,#3982,#2538,.T.);
#4833=EDGE_CURVE('',#3982,#3982,#3400,.T.);
#4834=EDGE_CURVE('',#3983,#3983,#3401,.T.);
#4835=EDGE_CURVE('',#3983,#3984,#2539,.T.);
#4836=EDGE_CURVE('',#3984,#3984,#3402,.T.);
#4837=EDGE_CURVE('',#3984,#3985,#2540,.T.);
#4838=EDGE_CURVE('',#3985,#3985,#3403,.T.);
#4839=EDGE_CURVE('',#3986,#3986,#3404,.T.);
#4840=EDGE_CURVE('',#3986,#3978,#2541,.T.);
#4841=EDGE_CURVE('',#3987,#3987,#3405,.T.);
#4842=EDGE_CURVE('',#3987,#3983,#2542,.T.);
#6402=ORIENTED_EDGE('',*,*,#4827,.F.);
#6403=ORIENTED_EDGE('',*,*,#4828,.F.);
#6404=ORIENTED_EDGE('',*,*,#4829,.T.);
#6405=ORIENTED_EDGE('',*,*,#4830,.F.);
#6406=ORIENTED_EDGE('',*,*,#4831,.F.);
#6407=ORIENTED_EDGE('',*,*,#4829,.F.);
#6408=ORIENTED_EDGE('',*,*,#4830,.T.);
#6409=ORIENTED_EDGE('',*,*,#4831,.T.);
#6410=ORIENTED_EDGE('',*,*,#4832,.T.);
#6411=ORIENTED_EDGE('',*,*,#4833,.T.);
#6412=ORIENTED_EDGE('',*,*,#4832,.F.);
#6413=ORIENTED_EDGE('',*,*,#4834,.T.);
#6414=ORIENTED_EDGE('',*,*,#4835,.T.);
#6415=ORIENTED_EDGE('',*,*,#4836,.F.);
#6416=ORIENTED_EDGE('',*,*,#4835,.F.);
#6417=ORIENTED_EDGE('',*,*,#4836,.T.);
#6418=ORIENTED_EDGE('',*,*,#4837,.T.);
#6419=ORIENTED_EDGE('',*,*,#4838,.F.);
#6420=ORIENTED_EDGE('',*,*,#4837,.F.);
#6421=ORIENTED_EDGE('',*,*,#4833,.F.);
#6422=ORIENTED_EDGE('',*,*,#4838,.T.);
#6423=ORIENTED_EDGE('',*,*,#4839,.F.);
#6424=ORIENTED_EDGE('',*,*,#4840,.T.);
#6425=ORIENTED_EDGE('',*,*,#4827,.T.);
#6426=ORIENTED_EDGE('',*,*,#4828,.T.);
#6427=ORIENTED_EDGE('',*,*,#4840,.F.);
#6428=ORIENTED_EDGE('',*,*,#4839,.T.);
#6429=ORIENTED_EDGE('',*,*,#4841,.F.);
#6430=ORIENTED_EDGE('',*,*,#4841,.T.);
#6431=ORIENTED_EDGE('',*,*,#4842,.T.);
#6432=ORIENTED_EDGE('',*,*,#4834,.F.);
#6433=ORIENTED_EDGE('',*,*,#4842,.F.);
#7162=CYLINDRICAL_SURFACE('',#8758,1.63531);
#7163=CYLINDRICAL_SURFACE('',#8760,1.);
#7164=CYLINDRICAL_SURFACE('',#8766,1.63531);
#7495=ADVANCED_FACE('',(#1384),#427,.F.);
#7496=ADVANCED_FACE('',(#1385),#7162,.T.);
#7497=ADVANCED_FACE('',(#1386),#7163,.F.);
#7498=ADVANCED_FACE('',(#1387),#436,.F.);
#7499=ADVANCED_FACE('',(#1388,#823),#1018,.T.);
#7500=ADVANCED_FACE('',(#1389),#7164,.T.);
#7501=ADVANCED_FACE('',(#1390,#824),#1019,.T.);
#7502=ADVANCED_FACE('',(#1391),#437,.F.);
#7684=CLOSED_SHELL('',(#7495,#7496,#7497,#7498,#7499,#7500,#7501,#7502));
#8751=AXIS2_PLACEMENT_3D('',#13319,#10703,#10704);
#8752=AXIS2_PLACEMENT_3D('',#13320,#10705,#10706);
#8753=AXIS2_PLACEMENT_3D('',#13323,#10707,#10708);
#8754=AXIS2_PLACEMENT_3D('',#13324,#10709,#10710);
#8755=AXIS2_PLACEMENT_3D('',#13326,#10711,#10712);
#8756=AXIS2_PLACEMENT_3D('',#13328,#10713,#10714);
#8757=AXIS2_PLACEMENT_3D('',#13329,#10715,#10716);
#8758=AXIS2_PLACEMENT_3D('',#13330,#10717,#10718);
#8759=AXIS2_PLACEMENT_3D('',#13333,#10720,#10721);
#8760=AXIS2_PLACEMENT_3D('',#13334,#10722,#10723);
#8761=AXIS2_PLACEMENT_3D('',#13336,#10724,#10725);
#8762=AXIS2_PLACEMENT_3D('',#13339,#10727,#10728);
#8763=AXIS2_PLACEMENT_3D('',#13340,#10729,#10730);
#8764=AXIS2_PLACEMENT_3D('',#13343,#10732,#10733);
#8765=AXIS2_PLACEMENT_3D('',#13344,#10734,#10735);
#8766=AXIS2_PLACEMENT_3D('',#13345,#10736,#10737);
#8767=AXIS2_PLACEMENT_3D('',#13347,#10738,#10739);
#8768=AXIS2_PLACEMENT_3D('',#13349,#10741,#10742);
#8769=AXIS2_PLACEMENT_3D('',#13351,#10743,#10744);
#8770=AXIS2_PLACEMENT_3D('',#13352,#10745,#10746);
#10703=DIRECTION('axis',(0.,0.,1.));
#10704=DIRECTION('refdir',(1.,0.,0.));
#10705=DIRECTION('center_axis',(0.,-1.,0.));
#10706=DIRECTION('ref_axis',(0.,0.,-1.));
#10707=DIRECTION('center_axis',(0.,-1.,0.));
#10708=DIRECTION('ref_axis',(1.,0.,0.));
#10709=DIRECTION('center_axis',(0.,-1.,0.));
#10710=DIRECTION('ref_axis',(1.,0.,0.));
#10711=DIRECTION('center_axis',(1.,0.,1.22464679914735E-16));
#10712=DIRECTION('ref_axis',(-1.22464679914735E-16,0.,1.));
#10713=DIRECTION('center_axis',(0.,1.,0.));
#10714=DIRECTION('ref_axis',(1.,0.,0.));
#10715=DIRECTION('center_axis',(0.,1.,0.));
#10716=DIRECTION('ref_axis',(1.,0.,0.));
#10717=DIRECTION('center_axis',(0.,-1.,0.));
#10718=DIRECTION('ref_axis',(1.,0.,0.));
#10719=DIRECTION('',(0.,1.,0.));
#10720=DIRECTION('center_axis',(0.,-1.,0.));
#10721=DIRECTION('ref_axis',(1.,0.,0.));
#10722=DIRECTION('center_axis',(0.,-1.,0.));
#10723=DIRECTION('ref_axis',(1.,0.,0.));
#10724=DIRECTION('center_axis',(0.,-1.,0.));
#10725=DIRECTION('ref_axis',(1.,0.,0.));
#10726=DIRECTION('',(0.,1.,0.));
#10727=DIRECTION('center_axis',(0.,-1.,0.));
#10728=DIRECTION('ref_axis',(1.,0.,0.));
#10729=DIRECTION('center_axis',(0.,1.,0.));
#10730=DIRECTION('ref_axis',(1.,0.,0.));
#10731=DIRECTION('',(-0.707106781186548,0.707106781186547,-8.65956056235494E-17));
#10732=DIRECTION('center_axis',(0.,-1.,0.));
#10733=DIRECTION('ref_axis',(1.,0.,0.));
#10734=DIRECTION('center_axis',(0.,1.,0.));
#10735=DIRECTION('ref_axis',(0.,0.,1.));
#10736=DIRECTION('center_axis',(0.,-1.,0.));
#10737=DIRECTION('ref_axis',(1.,0.,0.));
#10738=DIRECTION('center_axis',(0.,-1.,0.));
#10739=DIRECTION('ref_axis',(1.,0.,0.));
#10740=DIRECTION('',(0.,1.,0.));
#10741=DIRECTION('center_axis',(0.,-1.,0.));
#10742=DIRECTION('ref_axis',(0.,0.,-1.));
#10743=DIRECTION('center_axis',(0.,-1.,0.));
#10744=DIRECTION('ref_axis',(1.,0.,0.));
#10745=DIRECTION('center_axis',(0.,-1.,0.));
#10746=DIRECTION('ref_axis',(1.,0.,0.));
#10747=DIRECTION('',(0.707106781186548,0.707106781186547,8.65956056235494E-17));
#13319=CARTESIAN_POINT('',(0.,0.,0.));
#13320=CARTESIAN_POINT('Origin',(0.,0.,0.));
#13321=CARTESIAN_POINT('',(-1.63531,-0.410863395882378,-2.00267715711366E-16));
#13322=CARTESIAN_POINT('',(-2.00267715711366E-16,-0.410863395882378,1.63531));
#13323=CARTESIAN_POINT('Origin',(0.,-0.410863395882378,0.));
#13324=CARTESIAN_POINT('Origin',(0.,-0.410863395882378,0.));
#13325=CARTESIAN_POINT('',(-2.00267715711366E-16,0.410863395882378,1.63531));
#13326=CARTESIAN_POINT('Origin',(-2.05128338857182E-16,0.,1.675));
#13327=CARTESIAN_POINT('',(-1.63531,0.410863395882378,2.00267715711366E-16));
#13328=CARTESIAN_POINT('Origin',(0.,0.410863395882378,0.));
#13329=CARTESIAN_POINT('Origin',(0.,0.410863395882378,0.));
#13330=CARTESIAN_POINT('Origin',(0.,0.,0.));
#13331=CARTESIAN_POINT('',(-1.63531,0.7,-2.00267715711366E-16));
#13332=CARTESIAN_POINT('',(-1.63531,0.,-2.00267715711366E-16));
#13333=CARTESIAN_POINT('Origin',(0.,0.7,0.));
#13334=CARTESIAN_POINT('Origin',(0.,0.,0.));
#13335=CARTESIAN_POINT('',(-1.,-0.6,-1.22464679914735E-16));
#13336=CARTESIAN_POINT('Origin',(0.,-0.6,0.));
#13337=CARTESIAN_POINT('',(-1.,0.6,-1.22464679914735E-16));
#13338=CARTESIAN_POINT('',(-1.,0.,-1.22464679914735E-16));
#13339=CARTESIAN_POINT('Origin',(0.,0.6,0.));
#13340=CARTESIAN_POINT('Origin',(0.,0.65,0.));
#13341=CARTESIAN_POINT('',(-1.1,0.7,-1.34711147906209E-16));
#13342=CARTESIAN_POINT('',(-1.05,0.65,-1.28587913910472E-16));
#13343=CARTESIAN_POINT('Origin',(0.,0.7,0.));
#13344=CARTESIAN_POINT('Origin',(1.63531,0.7,0.));
#13345=CARTESIAN_POINT('Origin',(0.,0.,0.));
#13346=CARTESIAN_POINT('',(-1.63531,-0.7,-2.00267715711366E-16));
#13347=CARTESIAN_POINT('Origin',(0.,-0.7,0.));
#13348=CARTESIAN_POINT('',(-1.63531,0.,-2.00267715711366E-16));
#13349=CARTESIAN_POINT('Origin',(1.1,-0.7,0.));
#13350=CARTESIAN_POINT('',(-1.1,-0.7,-1.34711147906209E-16));
#13351=CARTESIAN_POINT('Origin',(0.,-0.7,0.));
#13352=CARTESIAN_POINT('Origin',(0.,-0.65,0.));
#13353=CARTESIAN_POINT('',(-1.05,-0.65,-1.28587913910472E-16));
#14758=UNCERTAINTY_MEASURE_WITH_UNIT(LENGTH_MEASURE(0.001),#14823,
'DISTANCE_ACCURACY_VALUE',
'Maximum model space distance between geometric entities at asserted c
onnectivities');
#14777=UNCERTAINTY_MEASURE_WITH_UNIT(LENGTH_MEASURE(0.001),#14823,
'DISTANCE_ACCURACY_VALUE',
'Maximum model space distance between geometric entities at asserted c
onnectivities');
#14803=(
GEOMETRIC_REPRESENTATION_CONTEXT(3)
GLOBAL_UNCERTAINTY_ASSIGNED_CONTEXT((#14758))
GLOBAL_UNIT_ASSIGNED_CONTEXT((#14823,#14825,#14826))
REPRESENTATION_CONTEXT('','3D')
);
#14822=(
GEOMETRIC_REPRESENTATION_CONTEXT(3)
GLOBAL_UNCERTAINTY_ASSIGNED_CONTEXT((#14777))
GLOBAL_UNIT_ASSIGNED_CONTEXT((#14823,#14825,#14826))
REPRESENTATION_CONTEXT('','3D')
);
#14823=(
LENGTH_UNIT()
NAMED_UNIT(*)
SI_UNIT(.CENTI.,.METRE.)
);
#14825=(
NAMED_UNIT(*)
PLANE_ANGLE_UNIT()
SI_UNIT($,.RADIAN.)
);
#14826=(
NAMED_UNIT(*)
SI_UNIT($,.STERADIAN.)
SOLID_ANGLE_UNIT()
);
#14852=SHAPE_DEFINITION_REPRESENTATION(#14901,#15023);
#14901=PRODUCT_DEFINITION_SHAPE('',$,#15068);
#15023=SHAPE_REPRESENTATION('',(#8751),#14803);
#15042=PRODUCT_DEFINITION_CONTEXT('part definition',#15176,'design');
#15068=PRODUCT_DEFINITION('Inner ring (1)','Inner ring (1)',#15112,#15042);
#15112=PRODUCT_DEFINITION_FORMATION('',$,#15203);
#15176=APPLICATION_CONTEXT(
'Core Data for Automotive Mechanical Design Process');
#15177=PRODUCT_CONTEXT('part definition',#15176,'mechanical');
#15203=PRODUCT('Inner ring (1)','Inner ring (1)','Inner ring (1)',(#15177));
#15278=COLOUR_RGB('Grey',0.48,0.52,0.57);
#15279=FILL_AREA_STYLE_COLOUR('',#15278);
#15280=FILL_AREA_STYLE('',(#15279));
#15281=SURFACE_STYLE_FILL_AREA(#15280);
#15282=SURFACE_SIDE_STYLE('',(#15281));
#15283=SURFACE_STYLE_USAGE(.BOTH.,#15282);
#15284=PRESENTATION_STYLE_ASSIGNMENT((#15283));
ENDSEC;
END-ISO-10303-21;
